ISO-10303-21;
HEADER;
/* Generated by software containing ST-Developer
 * from STEP Tools, Inc. (www.steptools.com) 
 */

FILE_DESCRIPTION(
/* description */ (''),
/* implementation_level */ '2;1');

FILE_NAME(
/* name */ '08_Grease_Seal_1.719x2.565_Dexter_10-36.step',
/* time_stamp */ '2026-10-25T01:26:34-07:00',
/* author */ (''),
/* organization */ (''),
/* preprocessor_version */ 'ST-DEVELOPER v20.2',
/* originating_system */ 'Autodesk Translation Framework v15.15.0.0',
/* authorisation */ '');

FILE_SCHEMA (('AUTOMOTIVE_DESIGN { 1 0 10303 214 3 1 1 }'));
ENDSEC;

DATA;
#10=MECHANICAL_DESIGN_GEOMETRIC_PRESENTATION_REPRESENTATION('',(#323),#71628);
#95=TOROIDAL_SURFACE('',#36358,25.4,0.8);
#297=SHAPE_REPRESENTATION_RELATIONSHIP('SRR','None',#71685,#310);
#310=ADVANCED_BREP_SHAPE_REPRESENTATION('',(#336),#71617);
#323=STYLED_ITEM('',(#71825),#336);
#336=MANIFOLD_SOLID_BREP('Body1',#34210);
#1234=FACE_BOUND('',#6730,.T.);
#1235=FACE_BOUND('',#6734,.T.);
#1236=FACE_BOUND('',#6738,.T.);
#1237=FACE_BOUND('',#6747,.T.);
#2591=PLANE('',#36346);
#2592=PLANE('',#36354);
#2593=PLANE('',#36362);
#2594=PLANE('',#36376);
#3056=CYLINDRICAL_SURFACE('',#36348,24.5);
#3057=CYLINDRICAL_SURFACE('',#36356,29.4);
#3058=CYLINDRICAL_SURFACE('',#36366,32.585);
#3059=CYLINDRICAL_SURFACE('',#36373,21.8413);
#4529=FACE_OUTER_BOUND('',#6728,.T.);
#4530=FACE_OUTER_BOUND('',#6729,.T.);
#4531=FACE_OUTER_BOUND('',#6731,.T.);
#4532=FACE_OUTER_BOUND('',#6732,.T.);
#4533=FACE_OUTER_BOUND('',#6733,.T.);
#4534=FACE_OUTER_BOUND('',#6735,.T.);
#4535=FACE_OUTER_BOUND('',#6736,.T.);
#4536=FACE_OUTER_BOUND('',#6737,.T.);
#4537=FACE_OUTER_BOUND('',#6739,.T.);
#4538=FACE_OUTER_BOUND('',#6740,.T.);
#4539=FACE_OUTER_BOUND('',#6741,.T.);
#4540=FACE_OUTER_BOUND('',#6742,.T.);
#4541=FACE_OUTER_BOUND('',#6743,.T.);
#4542=FACE_OUTER_BOUND('',#6744,.T.);
#4543=FACE_OUTER_BOUND('',#6745,.T.);
#4544=FACE_OUTER_BOUND('',#6746,.T.);
#6728=EDGE_LOOP('',(#28512,#28513,#28514,#28515,#28516));
#6729=EDGE_LOOP('',(#28517));
#6730=EDGE_LOOP('',(#28518));
#6731=EDGE_LOOP('',(#28519,#28520,#28521,#28522,#28523));
#6732=EDGE_LOOP('',(#28524,#28525,#28526,#28527,#28528));
#6733=EDGE_LOOP('',(#28529));
#6734=EDGE_LOOP('',(#28530));
#6735=EDGE_LOOP('',(#28531,#28532,#28533,#28534,#28535));
#6736=EDGE_LOOP('',(#28536,#28537,#28538,#28539));
#6737=EDGE_LOOP('',(#28540));
#6738=EDGE_LOOP('',(#28541));
#6739=EDGE_LOOP('',(#28542,#28543,#28544,#28545));
#6740=EDGE_LOOP('',(#28546,#28547,#28548,#28549));
#6741=EDGE_LOOP('',(#28550,#28551,#28552,#28553));
#6742=EDGE_LOOP('',(#28554,#28555,#28556,#28557));
#6743=EDGE_LOOP('',(#28558,#28559,#28560,#28561));
#6744=EDGE_LOOP('',(#28562,#28563,#28564,#28565));
#6745=EDGE_LOOP('',(#28566,#28567,#28568,#28569));
#6746=EDGE_LOOP('',(#28570));
#6747=EDGE_LOOP('',(#28571));
#9918=LINE('',#57957,#12968);
#9919=LINE('',#57964,#12969);
#9920=LINE('',#57970,#12970);
#9921=LINE('',#57980,#12971);
#9922=LINE('',#57993,#12972);
#9923=LINE('',#57997,#12973);
#9924=LINE('',#57999,#12974);
#9925=LINE('',#58002,#12975);
#9926=LINE('',#58006,#12976);
#9927=LINE('',#58010,#12977);
#9928=LINE('',#58013,#12978);
#12968=VECTOR('',#44005,24.69);
#12969=VECTOR('',#44014,24.5);
#12970=VECTOR('',#44021,29.59);
#12971=VECTOR('',#44034,29.4);
#12972=VECTOR('',#44051,32.385);
#12973=VECTOR('',#44056,32.585);
#12974=VECTOR('',#44059,32.385);
#12975=VECTOR('',#44062,23.95);
#12976=VECTOR('',#44067,22.62065);
#12977=VECTOR('',#44072,21.8413);
#12978=VECTOR('',#44077,22.77065);
#13941=CIRCLE('',#36343,24.5);
#13942=CIRCLE('',#36344,24.5);
#13943=CIRCLE('',#36345,24.88);
#13944=CIRCLE('',#36347,32.185);
#13945=CIRCLE('',#36349,24.5);
#13946=CIRCLE('',#36351,29.78);
#13947=CIRCLE('',#36352,29.4);
#13948=CIRCLE('',#36353,29.4);
#13949=CIRCLE('',#36355,32.185);
#13950=CIRCLE('',#36357,29.4);
#13951=CIRCLE('',#36359,26.2);
#13952=CIRCLE('',#36360,0.8);
#13953=CIRCLE('',#36361,24.6);
#13954=CIRCLE('',#36363,23.7);
#13955=CIRCLE('',#36365,32.585);
#13956=CIRCLE('',#36367,32.585);
#13957=CIRCLE('',#36370,23.4);
#13958=CIRCLE('',#36372,21.8413);
#13959=CIRCLE('',#36374,21.8413);
#16345=VERTEX_POINT('',#57952);
#16346=VERTEX_POINT('',#57953);
#16347=VERTEX_POINT('',#57956);
#16348=VERTEX_POINT('',#57960);
#16349=VERTEX_POINT('',#57963);
#16350=VERTEX_POINT('',#57967);
#16351=VERTEX_POINT('',#57969);
#16352=VERTEX_POINT('',#57971);
#16353=VERTEX_POINT('',#57975);
#16354=VERTEX_POINT('',#57978);
#16355=VERTEX_POINT('',#57982);
#16356=VERTEX_POINT('',#57984);
#16357=VERTEX_POINT('',#57988);
#16358=VERTEX_POINT('',#57991);
#16359=VERTEX_POINT('',#57995);
#16360=VERTEX_POINT('',#58001);
#16361=VERTEX_POINT('',#58005);
#16362=VERTEX_POINT('',#58009);
#20570=EDGE_CURVE('',#16345,#16346,#13941,.T.);
#20571=EDGE_CURVE('',#16346,#16345,#13942,.T.);
#20572=EDGE_CURVE('',#16345,#16347,#9918,.T.);
#20573=EDGE_CURVE('',#16347,#16347,#13943,.T.);
#20574=EDGE_CURVE('',#16348,#16348,#13944,.T.);
#20575=EDGE_CURVE('',#16346,#16349,#9919,.T.);
#20576=EDGE_CURVE('',#16349,#16349,#13945,.T.);
#20577=EDGE_CURVE('',#16350,#16350,#13946,.T.);
#20578=EDGE_CURVE('',#16350,#16351,#9920,.T.);
#20579=EDGE_CURVE('',#16351,#16352,#13947,.T.);
#20580=EDGE_CURVE('',#16352,#16351,#13948,.T.);
#20581=EDGE_CURVE('',#16353,#16353,#13949,.T.);
#20582=EDGE_CURVE('',#16354,#16354,#13950,.T.);
#20583=EDGE_CURVE('',#16354,#16352,#9921,.T.);
#20584=EDGE_CURVE('',#16355,#16355,#13951,.T.);
#20585=EDGE_CURVE('',#16355,#16356,#13952,.T.);
#20586=EDGE_CURVE('',#16356,#16356,#13953,.T.);
#20587=EDGE_CURVE('',#16357,#16357,#13954,.T.);
#20588=EDGE_CURVE('',#16358,#16358,#13955,.T.);
#20589=EDGE_CURVE('',#16358,#16353,#9922,.T.);
#20590=EDGE_CURVE('',#16359,#16359,#13956,.T.);
#20591=EDGE_CURVE('',#16359,#16358,#9923,.T.);
#20592=EDGE_CURVE('',#16348,#16359,#9924,.T.);
#20593=EDGE_CURVE('',#16349,#16360,#9925,.T.);
#20594=EDGE_CURVE('',#16360,#16360,#13957,.T.);
#20595=EDGE_CURVE('',#16360,#16361,#9926,.T.);
#20596=EDGE_CURVE('',#16361,#16361,#13958,.T.);
#20597=EDGE_CURVE('',#16361,#16362,#9927,.T.);
#20598=EDGE_CURVE('',#16362,#16362,#13959,.T.);
#20599=EDGE_CURVE('',#16362,#16357,#9928,.T.);
#28512=ORIENTED_EDGE('',*,*,#20570,.T.);
#28513=ORIENTED_EDGE('',*,*,#20571,.T.);
#28514=ORIENTED_EDGE('',*,*,#20572,.T.);
#28515=ORIENTED_EDGE('',*,*,#20573,.T.);
#28516=ORIENTED_EDGE('',*,*,#20572,.F.);
#28517=ORIENTED_EDGE('',*,*,#20574,.T.);
#28518=ORIENTED_EDGE('',*,*,#20573,.F.);
#28519=ORIENTED_EDGE('',*,*,#20570,.F.);
#28520=ORIENTED_EDGE('',*,*,#20571,.F.);
#28521=ORIENTED_EDGE('',*,*,#20575,.T.);
#28522=ORIENTED_EDGE('',*,*,#20576,.F.);
#28523=ORIENTED_EDGE('',*,*,#20575,.F.);
#28524=ORIENTED_EDGE('',*,*,#20577,.T.);
#28525=ORIENTED_EDGE('',*,*,#20578,.T.);
#28526=ORIENTED_EDGE('',*,*,#20579,.T.);
#28527=ORIENTED_EDGE('',*,*,#20580,.T.);
#28528=ORIENTED_EDGE('',*,*,#20578,.F.);
#28529=ORIENTED_EDGE('',*,*,#20581,.F.);
#28530=ORIENTED_EDGE('',*,*,#20577,.F.);
#28531=ORIENTED_EDGE('',*,*,#20582,.T.);
#28532=ORIENTED_EDGE('',*,*,#20583,.T.);
#28533=ORIENTED_EDGE('',*,*,#20579,.F.);
#28534=ORIENTED_EDGE('',*,*,#20580,.F.);
#28535=ORIENTED_EDGE('',*,*,#20583,.F.);
#28536=ORIENTED_EDGE('',*,*,#20584,.F.);
#28537=ORIENTED_EDGE('',*,*,#20585,.T.);
#28538=ORIENTED_EDGE('',*,*,#20586,.F.);
#28539=ORIENTED_EDGE('',*,*,#20585,.F.);
#28540=ORIENTED_EDGE('',*,*,#20586,.T.);
#28541=ORIENTED_EDGE('',*,*,#20587,.T.);
#28542=ORIENTED_EDGE('',*,*,#20588,.F.);
#28543=ORIENTED_EDGE('',*,*,#20589,.T.);
#28544=ORIENTED_EDGE('',*,*,#20581,.T.);
#28545=ORIENTED_EDGE('',*,*,#20589,.F.);
#28546=ORIENTED_EDGE('',*,*,#20590,.F.);
#28547=ORIENTED_EDGE('',*,*,#20591,.T.);
#28548=ORIENTED_EDGE('',*,*,#20588,.T.);
#28549=ORIENTED_EDGE('',*,*,#20591,.F.);
#28550=ORIENTED_EDGE('',*,*,#20574,.F.);
#28551=ORIENTED_EDGE('',*,*,#20592,.T.);
#28552=ORIENTED_EDGE('',*,*,#20590,.T.);
#28553=ORIENTED_EDGE('',*,*,#20592,.F.);
#28554=ORIENTED_EDGE('',*,*,#20576,.T.);
#28555=ORIENTED_EDGE('',*,*,#20593,.T.);
#28556=ORIENTED_EDGE('',*,*,#20594,.F.);
#28557=ORIENTED_EDGE('',*,*,#20593,.F.);
#28558=ORIENTED_EDGE('',*,*,#20594,.T.);
#28559=ORIENTED_EDGE('',*,*,#20595,.T.);
#28560=ORIENTED_EDGE('',*,*,#20596,.F.);
#28561=ORIENTED_EDGE('',*,*,#20595,.F.);
#28562=ORIENTED_EDGE('',*,*,#20596,.T.);
#28563=ORIENTED_EDGE('',*,*,#20597,.T.);
#28564=ORIENTED_EDGE('',*,*,#20598,.F.);
#28565=ORIENTED_EDGE('',*,*,#20597,.F.);
#28566=ORIENTED_EDGE('',*,*,#20598,.T.);
#28567=ORIENTED_EDGE('',*,*,#20599,.T.);
#28568=ORIENTED_EDGE('',*,*,#20587,.F.);
#28569=ORIENTED_EDGE('',*,*,#20599,.F.);
#28570=ORIENTED_EDGE('',*,*,#20582,.F.);
#28571=ORIENTED_EDGE('',*,*,#20584,.T.);
#31986=CONICAL_SURFACE('',#36342,24.69,0.785398163397445);
#31987=CONICAL_SURFACE('',#36350,29.59,0.785398163397446);
#31988=CONICAL_SURFACE('',#36364,32.385,0.785398163397449);
#31989=CONICAL_SURFACE('',#36368,32.385,0.785398163397448);
#31990=CONICAL_SURFACE('',#36369,23.95,0.548549402450529);
#31991=CONICAL_SURFACE('',#36371,22.62065,0.687037904785236);
#31992=CONICAL_SURFACE('',#36375,22.77065,0.801440737031442);
#33503=ADVANCED_FACE('',(#4529),#31986,.F.);
#33504=ADVANCED_FACE('',(#4530,#1234),#2591,.T.);
#33505=ADVANCED_FACE('',(#4531),#3056,.F.);
#33506=ADVANCED_FACE('',(#4532),#31987,.F.);
#33507=ADVANCED_FACE('',(#4533,#1235),#2592,.T.);
#33508=ADVANCED_FACE('',(#4534),#3057,.F.);
#33509=ADVANCED_FACE('',(#4535),#95,.F.);
#33510=ADVANCED_FACE('',(#4536,#1236),#2593,.T.);
#33511=ADVANCED_FACE('',(#4537),#31988,.T.);
#33512=ADVANCED_FACE('',(#4538),#3058,.T.);
#33513=ADVANCED_FACE('',(#4539),#31989,.T.);
#33514=ADVANCED_FACE('',(#4540),#31990,.F.);
#33515=ADVANCED_FACE('',(#4541),#31991,.F.);
#33516=ADVANCED_FACE('',(#4542),#3059,.F.);
#33517=ADVANCED_FACE('',(#4543),#31992,.F.);
#33518=ADVANCED_FACE('',(#4544,#1237),#2594,.T.);
#34210=CLOSED_SHELL('',(#33503,#33504,#33505,#33506,#33507,#33508,#33509,
#33510,#33511,#33512,#33513,#33514,#33515,#33516,#33517,#33518));
#36341=AXIS2_PLACEMENT_3D('',#57950,#43997,#43998);
#36342=AXIS2_PLACEMENT_3D('',#57951,#43999,#44000);
#36343=AXIS2_PLACEMENT_3D('',#57954,#44001,#44002);
#36344=AXIS2_PLACEMENT_3D('',#57955,#44003,#44004);
#36345=AXIS2_PLACEMENT_3D('',#57958,#44006,#44007);
#36346=AXIS2_PLACEMENT_3D('',#57959,#44008,#44009);
#36347=AXIS2_PLACEMENT_3D('',#57961,#44010,#44011);
#36348=AXIS2_PLACEMENT_3D('',#57962,#44012,#44013);
#36349=AXIS2_PLACEMENT_3D('',#57965,#44015,#44016);
#36350=AXIS2_PLACEMENT_3D('',#57966,#44017,#44018);
#36351=AXIS2_PLACEMENT_3D('',#57968,#44019,#44020);
#36352=AXIS2_PLACEMENT_3D('',#57972,#44022,#44023);
#36353=AXIS2_PLACEMENT_3D('',#57973,#44024,#44025);
#36354=AXIS2_PLACEMENT_3D('',#57974,#44026,#44027);
#36355=AXIS2_PLACEMENT_3D('',#57976,#44028,#44029);
#36356=AXIS2_PLACEMENT_3D('',#57977,#44030,#44031);
#36357=AXIS2_PLACEMENT_3D('',#57979,#44032,#44033);
#36358=AXIS2_PLACEMENT_3D('',#57981,#44035,#44036);
#36359=AXIS2_PLACEMENT_3D('',#57983,#44037,#44038);
#36360=AXIS2_PLACEMENT_3D('',#57985,#44039,#44040);
#36361=AXIS2_PLACEMENT_3D('',#57986,#44041,#44042);
#36362=AXIS2_PLACEMENT_3D('',#57987,#44043,#44044);
#36363=AXIS2_PLACEMENT_3D('',#57989,#44045,#44046);
#36364=AXIS2_PLACEMENT_3D('',#57990,#44047,#44048);
#36365=AXIS2_PLACEMENT_3D('',#57992,#44049,#44050);
#36366=AXIS2_PLACEMENT_3D('',#57994,#44052,#44053);
#36367=AXIS2_PLACEMENT_3D('',#57996,#44054,#44055);
#36368=AXIS2_PLACEMENT_3D('',#57998,#44057,#44058);
#36369=AXIS2_PLACEMENT_3D('',#58000,#44060,#44061);
#36370=AXIS2_PLACEMENT_3D('',#58003,#44063,#44064);
#36371=AXIS2_PLACEMENT_3D('',#58004,#44065,#44066);
#36372=AXIS2_PLACEMENT_3D('',#58007,#44068,#44069);
#36373=AXIS2_PLACEMENT_3D('',#58008,#44070,#44071);
#36374=AXIS2_PLACEMENT_3D('',#58011,#44073,#44074);
#36375=AXIS2_PLACEMENT_3D('',#58012,#44075,#44076);
#36376=AXIS2_PLACEMENT_3D('',#58014,#44078,#44079);
#43997=DIRECTION('axis',(0.,0.,1.));
#43998=DIRECTION('refdir',(1.,0.,0.));
#43999=DIRECTION('center_axis',(1.,0.,0.));
#44000=DIRECTION('ref_axis',(0.,-1.,0.));
#44001=DIRECTION('center_axis',(-1.,0.,0.));
#44002=DIRECTION('ref_axis',(0.,-1.,0.));
#44003=DIRECTION('center_axis',(-1.,0.,0.));
#44004=DIRECTION('ref_axis',(0.,-1.,0.));
#44005=DIRECTION('',(0.707106781186549,0.707106781186545,-8.65956056235491E-17));
#44006=DIRECTION('center_axis',(1.,0.,0.));
#44007=DIRECTION('ref_axis',(0.,-1.,0.));
#44008=DIRECTION('center_axis',(1.,0.,0.));
#44009=DIRECTION('ref_axis',(0.,0.,-1.));
#44010=DIRECTION('center_axis',(1.,0.,0.));
#44011=DIRECTION('ref_axis',(0.,0.,-1.));
#44012=DIRECTION('center_axis',(1.,0.,0.));
#44013=DIRECTION('ref_axis',(0.,1.,0.));
#44014=DIRECTION('',(-1.,0.,0.));
#44015=DIRECTION('center_axis',(1.,0.,0.));
#44016=DIRECTION('ref_axis',(0.,0.,-1.));
#44017=DIRECTION('center_axis',(-1.,0.,0.));
#44018=DIRECTION('ref_axis',(0.,-1.,0.));
#44019=DIRECTION('center_axis',(-1.,0.,0.));
#44020=DIRECTION('ref_axis',(0.,-1.,0.));
#44021=DIRECTION('',(0.707106781186549,-0.707106781186546,8.65956056235491E-17));
#44022=DIRECTION('center_axis',(1.,0.,0.));
#44023=DIRECTION('ref_axis',(0.,-1.,0.));
#44024=DIRECTION('center_axis',(1.,0.,0.));
#44025=DIRECTION('ref_axis',(0.,-1.,0.));
#44026=DIRECTION('center_axis',(-1.,0.,0.));
#44027=DIRECTION('ref_axis',(0.,0.,1.));
#44028=DIRECTION('center_axis',(1.,0.,0.));
#44029=DIRECTION('ref_axis',(0.,0.,-1.));
#44030=DIRECTION('center_axis',(1.,0.,0.));
#44031=DIRECTION('ref_axis',(0.,1.,0.));
#44032=DIRECTION('center_axis',(1.,0.,0.));
#44033=DIRECTION('ref_axis',(0.,0.,-1.));
#44034=DIRECTION('',(-1.,0.,0.));
#44035=DIRECTION('center_axis',(1.,0.,0.));
#44036=DIRECTION('ref_axis',(0.,0.,-1.));
#44037=DIRECTION('center_axis',(1.,0.,0.));
#44038=DIRECTION('ref_axis',(0.,0.,-1.));
#44039=DIRECTION('center_axis',(0.,1.,1.22464679914735E-16));
#44040=DIRECTION('ref_axis',(0.,-1.22464679914735E-16,1.));
#44041=DIRECTION('center_axis',(-1.,0.,0.));
#44042=DIRECTION('ref_axis',(0.,0.,-1.));
#44043=DIRECTION('center_axis',(-1.,0.,0.));
#44044=DIRECTION('ref_axis',(0.,0.,1.));
#44045=DIRECTION('center_axis',(1.,0.,0.));
#44046=DIRECTION('ref_axis',(0.,0.,-1.));
#44047=DIRECTION('center_axis',(1.,0.,0.));
#44048=DIRECTION('ref_axis',(0.,1.,0.));
#44049=DIRECTION('center_axis',(1.,0.,0.));
#44050=DIRECTION('ref_axis',(0.,0.,-1.));
#44051=DIRECTION('',(-0.707106781186547,0.707106781186548,8.65956056235494E-17));
#44052=DIRECTION('center_axis',(1.,0.,0.));
#44053=DIRECTION('ref_axis',(0.,1.,0.));
#44054=DIRECTION('center_axis',(1.,0.,0.));
#44055=DIRECTION('ref_axis',(0.,0.,-1.));
#44056=DIRECTION('',(-1.,0.,0.));
#44057=DIRECTION('center_axis',(-1.,0.,0.));
#44058=DIRECTION('ref_axis',(0.,1.,0.));
#44059=DIRECTION('',(-0.707106781186547,-0.707106781186547,-8.65956056235493E-17));
#44060=DIRECTION('center_axis',(1.,0.,0.));
#44061=DIRECTION('ref_axis',(0.,1.,0.));
#44062=DIRECTION('',(-0.853281833651959,0.521450009453976,6.38592084993168E-17));
#44063=DIRECTION('center_axis',(1.,0.,0.));
#44064=DIRECTION('ref_axis',(0.,0.,-1.));
#44065=DIRECTION('center_axis',(1.,0.,0.));
#44066=DIRECTION('ref_axis',(0.,1.,0.));
#44067=DIRECTION('',(-0.773128112524476,0.634249888943105,7.76732096353738E-17));
#44068=DIRECTION('center_axis',(1.,0.,0.));
#44069=DIRECTION('ref_axis',(0.,0.,-1.));
#44070=DIRECTION('center_axis',(1.,0.,0.));
#44071=DIRECTION('ref_axis',(0.,1.,0.));
#44072=DIRECTION('',(-1.,0.,0.));
#44073=DIRECTION('center_axis',(1.,0.,0.));
#44074=DIRECTION('ref_axis',(0.,0.,-1.));
#44075=DIRECTION('center_axis',(-1.,0.,0.));
#44076=DIRECTION('ref_axis',(0.,1.,0.));
#44077=DIRECTION('',(-0.695672465134814,-0.718359117192266,-8.79736193507827E-17));
#44078=DIRECTION('center_axis',(-1.,0.,0.));
#44079=DIRECTION('ref_axis',(0.,0.,1.));
#57950=CARTESIAN_POINT('',(0.,0.,0.));
#57951=CARTESIAN_POINT('Origin',(9.31,0.,0.));
#57952=CARTESIAN_POINT('',(9.12,24.5,-3.00038465791102E-15));
#57953=CARTESIAN_POINT('',(9.12,-24.5,-3.00038465791102E-15));
#57954=CARTESIAN_POINT('Origin',(9.12,0.,0.));
#57955=CARTESIAN_POINT('Origin',(9.12,0.,0.));
#57956=CARTESIAN_POINT('',(9.5,24.88,3.04692123627861E-15));
#57957=CARTESIAN_POINT('',(9.31,24.69,-3.02365294709482E-15));
#57958=CARTESIAN_POINT('Origin',(9.5,0.,0.));
#57959=CARTESIAN_POINT('Origin',(9.5,24.5,0.));
#57960=CARTESIAN_POINT('',(9.5,-32.185,-3.94152572305576E-15));
#57961=CARTESIAN_POINT('Origin',(9.5,0.,0.));
#57962=CARTESIAN_POINT('Origin',(8.95,0.,0.));
#57963=CARTESIAN_POINT('',(8.4,-24.5,-3.00038465791102E-15));
#57964=CARTESIAN_POINT('',(8.95,-24.5,-3.00038465791102E-15));
#57965=CARTESIAN_POINT('Origin',(8.4,0.,0.));
#57966=CARTESIAN_POINT('Origin',(0.19,0.,0.));
#57967=CARTESIAN_POINT('',(0.,29.78,-3.64699816786082E-15));
#57968=CARTESIAN_POINT('Origin',(0.,0.,0.));
#57969=CARTESIAN_POINT('',(0.38,29.4,3.60046158949322E-15));
#57970=CARTESIAN_POINT('',(0.19,29.59,-3.62372987867702E-15));
#57971=CARTESIAN_POINT('',(0.38,-29.4,-3.60046158949322E-15));
#57972=CARTESIAN_POINT('Origin',(0.38,0.,0.));
#57973=CARTESIAN_POINT('Origin',(0.38,0.,0.));
#57974=CARTESIAN_POINT('Origin',(0.,32.185,0.));
#57975=CARTESIAN_POINT('',(-1.14491749414469E-15,-32.185,-3.94152572305576E-15));
#57976=CARTESIAN_POINT('Origin',(0.,0.,0.));
#57977=CARTESIAN_POINT('Origin',(0.8,0.,0.));
#57978=CARTESIAN_POINT('',(1.6,-29.4,-3.60046158949322E-15));
#57979=CARTESIAN_POINT('Origin',(1.6,0.,0.));
#57980=CARTESIAN_POINT('',(0.8,-29.4,-3.60046158949322E-15));
#57981=CARTESIAN_POINT('Origin',(1.6,0.,0.));
#57982=CARTESIAN_POINT('',(1.6,-3.20857461376607E-15,26.2));
#57983=CARTESIAN_POINT('Origin',(1.6,0.,0.));
#57984=CARTESIAN_POINT('',(1.6,3.01263112590249E-15,24.6));
#57985=CARTESIAN_POINT('Origin',(1.6,-3.11060286983428E-15,25.4));
#57986=CARTESIAN_POINT('Origin',(1.6,0.,0.));
#57987=CARTESIAN_POINT('Origin',(1.6,29.4,0.));
#57988=CARTESIAN_POINT('',(1.6,-23.7,-2.90241291397923E-15));
#57989=CARTESIAN_POINT('Origin',(1.6,0.,0.));
#57990=CARTESIAN_POINT('Origin',(0.2,0.,0.));
#57991=CARTESIAN_POINT('',(0.4,-32.585,-3.99051159502165E-15));
#57992=CARTESIAN_POINT('Origin',(0.4,0.,0.));
#57993=CARTESIAN_POINT('',(0.2,-32.385,-3.9660186590387E-15));
#57994=CARTESIAN_POINT('Origin',(4.75,0.,0.));
#57995=CARTESIAN_POINT('',(9.1,-32.585,-3.99051159502165E-15));
#57996=CARTESIAN_POINT('Origin',(9.1,0.,0.));
#57997=CARTESIAN_POINT('',(4.75,-32.585,-3.99051159502165E-15));
#57998=CARTESIAN_POINT('Origin',(9.3,0.,0.));
#57999=CARTESIAN_POINT('',(9.3,-32.385,-3.9660186590387E-15));
#58000=CARTESIAN_POINT('Origin',(7.5,0.,0.));
#58001=CARTESIAN_POINT('',(6.6,-23.4,-2.86567351000481E-15));
#58002=CARTESIAN_POINT('',(7.5,-23.95,-2.93302908395791E-15));
#58003=CARTESIAN_POINT('Origin',(6.6,0.,0.));
#58004=CARTESIAN_POINT('Origin',(5.65,0.,0.));
#58005=CARTESIAN_POINT('',(4.7,-21.8413,-2.67478781342171E-15));
#58006=CARTESIAN_POINT('',(5.65,-22.62065,-2.77023066171326E-15));
#58007=CARTESIAN_POINT('Origin',(4.7,0.,0.));
#58008=CARTESIAN_POINT('Origin',(4.05,0.,0.));
#58009=CARTESIAN_POINT('',(3.4,-21.8413,-2.67478781342171E-15));
#58010=CARTESIAN_POINT('',(4.05,-21.8413,-2.67478781342171E-15));
#58011=CARTESIAN_POINT('Origin',(3.4,0.,0.));
#58012=CARTESIAN_POINT('Origin',(2.5,0.,0.));
#58013=CARTESIAN_POINT('',(2.5,-22.77065,-2.78860036370047E-15));
#58014=CARTESIAN_POINT('Origin',(1.6,29.4,0.));
#71602=UNCERTAINTY_MEASURE_WITH_UNIT(LENGTH_MEASURE(0.01),#71629,
'DISTANCE_ACCURACY_VALUE',
'Maximum model space distance between geometric entities at asserted c
onnectivities');
#71613=UNCERTAINTY_MEASURE_WITH_UNIT(LENGTH_MEASURE(0.01),#71629,
'DISTANCE_ACCURACY_VALUE',
'Maximum model space distance between geometric entities at asserted c
onnectivities');
#71617=(
GEOMETRIC_REPRESENTATION_CONTEXT(3)
GLOBAL_UNCERTAINTY_ASSIGNED_CONTEXT((#71602))
GLOBAL_UNIT_ASSIGNED_CONTEXT((#71629,#71631,#71632))
REPRESENTATION_CONTEXT('','3D')
);
#71628=(
GEOMETRIC_REPRESENTATION_CONTEXT(3)
GLOBAL_UNCERTAINTY_ASSIGNED_CONTEXT((#71613))
GLOBAL_UNIT_ASSIGNED_CONTEXT((#71629,#71631,#71632))
REPRESENTATION_CONTEXT('','3D')
);
#71629=(
LENGTH_UNIT()
NAMED_UNIT(*)
SI_UNIT(.MILLI.,.METRE.)
);
#71631=(
NAMED_UNIT(*)
PLANE_ANGLE_UNIT()
SI_UNIT($,.RADIAN.)
);
#71632=(
NAMED_UNIT(*)
SI_UNIT($,.STERADIAN.)
SOLID_ANGLE_UNIT()
);
#71636=SHAPE_DEFINITION_REPRESENTATION(#71650,#71685);
#71650=PRODUCT_DEFINITION_SHAPE('',$,#71700);
#71685=SHAPE_REPRESENTATION('',(#36341),#71617);
#71696=PRODUCT_DEFINITION_CONTEXT('part definition',#71740,'design');
#71700=PRODUCT_DEFINITION('2026-10-25-00-23-52-198',
'08_Grease_Seal_1.719x2.565_Dexter_10-36',#71714,#71696);
#71714=PRODUCT_DEFINITION_FORMATION('',$,#71745);
#71740=APPLICATION_CONTEXT(
'Core Data for Automotive Mechanical Design Process');
#71741=PRODUCT_CONTEXT('part definition',#71740,'mechanical');
#71745=PRODUCT('2026-10-25-00-23-52-198',
'08_Grease_Seal_1.719x2.565_Dexter_10-36',$,(#71741));
#71819=COLOUR_RGB('Black',0.12,0.14,0.17);
#71820=FILL_AREA_STYLE_COLOUR('',#71819);
#71821=FILL_AREA_STYLE('',(#71820));
#71822=SURFACE_STYLE_FILL_AREA(#71821);
#71823=SURFACE_SIDE_STYLE('',(#71822));
#71824=SURFACE_STYLE_USAGE(.BOTH.,#71823);
#71825=PRESENTATION_STYLE_ASSIGNMENT((#71824));
ENDSEC;
END-ISO-10303-21;
